ISO-10303-21;
HEADER;
/* Generated by software containing ST-Developer
 * from STEP Tools, Inc. (www.steptools.com) 
 */

FILE_DESCRIPTION(
/* description */ ('Pedal-braked fixed caster'),
/* implementation_level */ '2;1');

FILE_NAME(
/* name */ 'Hex Bolt - M6 x 30 mm.step',
/* time_stamp */ '2026-10-28T03:26:52-07:00',
/* author */ (''),
/* organization */ (''),
/* preprocessor_version */ 'ST-DEVELOPER v20.2',
/* originating_system */ 'Autodesk Translation Framework v15.17.0.0',
/* authorisation */ '');

FILE_SCHEMA (('AUTOMOTIVE_DESIGN { 1 0 10303 214 3 1 1 }'));
ENDSEC;

DATA;
#10=MECHANICAL_DESIGN_GEOMETRIC_PRESENTATION_REPRESENTATION('',(#212),#5734);
#141=(
BOUNDED_CURVE()
B_SPLINE_CURVE(2,(#4882,#4883,#4884),.UNSPECIFIED.,.F.,.F.)
B_SPLINE_CURVE_WITH_KNOTS((3,3),(0.144988513094728,0.791574906712449),
 .UNSPECIFIED.)
CURVE()
GEOMETRIC_REPRESENTATION_ITEM()
RATIONAL_B_SPLINE_CURVE((1.09282032302755,1.26188021535082,1.09282032302931))
REPRESENTATION_ITEM('')
);
#142=(
BOUNDED_CURVE()
B_SPLINE_CURVE(2,(#4886,#4887,#4888),.UNSPECIFIED.,.F.,.F.)
B_SPLINE_CURVE_WITH_KNOTS((3,3),(0.144988513094728,0.791574906712449),
 .UNSPECIFIED.)
CURVE()
GEOMETRIC_REPRESENTATION_ITEM()
RATIONAL_B_SPLINE_CURVE((1.09282032302755,1.26188021535082,1.09282032302931))
REPRESENTATION_ITEM('')
);
#143=(
BOUNDED_CURVE()
B_SPLINE_CURVE(2,(#4890,#4891,#4892),.UNSPECIFIED.,.F.,.F.)
B_SPLINE_CURVE_WITH_KNOTS((3,3),(0.144988513094728,0.791574906712449),
 .UNSPECIFIED.)
CURVE()
GEOMETRIC_REPRESENTATION_ITEM()
RATIONAL_B_SPLINE_CURVE((1.09282032302755,1.26188021535082,1.09282032302931))
REPRESENTATION_ITEM('')
);
#144=(
BOUNDED_CURVE()
B_SPLINE_CURVE(2,(#4894,#4895,#4896),.UNSPECIFIED.,.F.,.F.)
B_SPLINE_CURVE_WITH_KNOTS((3,3),(0.144988513094728,0.791574906712449),
 .UNSPECIFIED.)
CURVE()
GEOMETRIC_REPRESENTATION_ITEM()
RATIONAL_B_SPLINE_CURVE((1.09282032302755,1.26188021535082,1.09282032302931))
REPRESENTATION_ITEM('')
);
#145=(
BOUNDED_CURVE()
B_SPLINE_CURVE(2,(#4898,#4899,#4900),.UNSPECIFIED.,.F.,.F.)
B_SPLINE_CURVE_WITH_KNOTS((3,3),(0.144988513094728,0.791574906712449),
 .UNSPECIFIED.)
CURVE()
GEOMETRIC_REPRESENTATION_ITEM()
RATIONAL_B_SPLINE_CURVE((1.09282032302755,1.26188021535082,1.09282032302931))
REPRESENTATION_ITEM('')
);
#146=(
BOUNDED_CURVE()
B_SPLINE_CURVE(2,(#4901,#4902,#4903),.UNSPECIFIED.,.F.,.F.)
B_SPLINE_CURVE_WITH_KNOTS((3,3),(0.144988513094727,0.791574906712449),
 .UNSPECIFIED.)
CURVE()
GEOMETRIC_REPRESENTATION_ITEM()
RATIONAL_B_SPLINE_CURVE((1.09282032302755,1.26188021535082,1.09282032302931))
REPRESENTATION_ITEM('')
);
#162=CONICAL_SURFACE('',#3330,0.27,0.785398163397448);
#163=CONICAL_SURFACE('',#3333,0.576175134594813,1.0471975511966);
#178=SHAPE_REPRESENTATION_RELATIONSHIP('SRR','None',#5816,#195);
#195=ADVANCED_BREP_SHAPE_REPRESENTATION('',(#235),#5720);
#212=STYLED_ITEM('',(#5991),#235);
#235=MANIFOLD_SOLID_BREP('Body1',#2994);
#272=CYLINDRICAL_SURFACE('',#3327,0.2942);
#320=FACE_BOUND('',#768,.T.);
#381=CIRCLE('',#3328,0.2942);
#382=CIRCLE('',#3329,0.2942);
#383=CIRCLE('',#3331,0.24);
#384=CIRCLE('',#3334,0.475);
#553=FACE_OUTER_BOUND('',#756,.T.);
#554=FACE_OUTER_BOUND('',#757,.T.);
#555=FACE_OUTER_BOUND('',#758,.T.);
#556=FACE_OUTER_BOUND('',#759,.T.);
#557=FACE_OUTER_BOUND('',#760,.T.);
#558=FACE_OUTER_BOUND('',#761,.T.);
#559=FACE_OUTER_BOUND('',#762,.T.);
#560=FACE_OUTER_BOUND('',#763,.T.);
#561=FACE_OUTER_BOUND('',#764,.T.);
#562=FACE_OUTER_BOUND('',#765,.T.);
#563=FACE_OUTER_BOUND('',#766,.T.);
#564=FACE_OUTER_BOUND('',#767,.T.);
#756=EDGE_LOOP('',(#2282,#2283,#2284,#2285));
#757=EDGE_LOOP('',(#2286,#2287,#2288,#2289));
#758=EDGE_LOOP('',(#2290));
#759=EDGE_LOOP('',(#2291,#2292,#2293,#2294,#2295,#2296,#2297,#2298,#2299));
#760=EDGE_LOOP('',(#2300,#2301,#2302,#2303));
#761=EDGE_LOOP('',(#2304,#2305,#2306,#2307));
#762=EDGE_LOOP('',(#2308,#2309,#2310,#2311));
#763=EDGE_LOOP('',(#2312,#2313,#2314,#2315));
#764=EDGE_LOOP('',(#2316,#2317,#2318,#2319));
#765=EDGE_LOOP('',(#2320,#2321,#2322,#2323));
#766=EDGE_LOOP('',(#2324));
#767=EDGE_LOOP('',(#2325,#2326,#2327,#2328,#2329,#2330));
#768=EDGE_LOOP('',(#2331));
#1007=LINE('',#4869,#1219);
#1008=LINE('',#4874,#1220);
#1009=LINE('',#4880,#1221);
#1010=LINE('',#4906,#1222);
#1011=LINE('',#4908,#1223);
#1012=LINE('',#4909,#1224);
#1013=LINE('',#4912,#1225);
#1014=LINE('',#4913,#1226);
#1015=LINE('',#4916,#1227);
#1016=LINE('',#4917,#1228);
#1017=LINE('',#4920,#1229);
#1018=LINE('',#4921,#1230);
#1019=LINE('',#4924,#1231);
#1020=LINE('',#4925,#1232);
#1021=LINE('',#4927,#1233);
#1219=VECTOR('',#3949,0.3);
#1220=VECTOR('',#3956,0.27);
#1221=VECTOR('',#3963,0.576175134594813);
#1222=VECTOR('',#3966,1.);
#1223=VECTOR('',#3967,1.);
#1224=VECTOR('',#3968,1.);
#1225=VECTOR('',#3971,1.);
#1226=VECTOR('',#3972,1.);
#1227=VECTOR('',#3975,1.);
#1228=VECTOR('',#3976,1.);
#1229=VECTOR('',#3979,1.);
#1230=VECTOR('',#3980,1.);
#1231=VECTOR('',#3983,1.);
#1232=VECTOR('',#3984,1.);
#1233=VECTOR('',#3987,1.);
#1414=VERTEX_POINT('',#4866);
#1415=VERTEX_POINT('',#4868);
#1416=VERTEX_POINT('',#4872);
#1417=VERTEX_POINT('',#4877);
#1418=VERTEX_POINT('',#4879);
#1419=VERTEX_POINT('',#4881);
#1420=VERTEX_POINT('',#4885);
#1421=VERTEX_POINT('',#4889);
#1422=VERTEX_POINT('',#4893);
#1423=VERTEX_POINT('',#4897);
#1424=VERTEX_POINT('',#4905);
#1425=VERTEX_POINT('',#4907);
#1426=VERTEX_POINT('',#4911);
#1427=VERTEX_POINT('',#4915);
#1428=VERTEX_POINT('',#4919);
#1429=VERTEX_POINT('',#4923);
#1731=EDGE_CURVE('',#1414,#1414,#381,.F.);
#1732=EDGE_CURVE('',#1414,#1415,#1007,.T.);
#1733=EDGE_CURVE('',#1415,#1415,#382,.F.);
#1734=EDGE_CURVE('',#1416,#1416,#383,.T.);
#1735=EDGE_CURVE('',#1416,#1414,#1008,.T.);
#1736=EDGE_CURVE('',#1417,#1417,#384,.T.);
#1737=EDGE_CURVE('',#1417,#1418,#1009,.T.);
#1738=EDGE_CURVE('',#1419,#1418,#141,.T.);
#1739=EDGE_CURVE('',#1420,#1419,#142,.T.);
#1740=EDGE_CURVE('',#1421,#1420,#143,.T.);
#1741=EDGE_CURVE('',#1422,#1421,#144,.T.);
#1742=EDGE_CURVE('',#1423,#1422,#145,.T.);
#1743=EDGE_CURVE('',#1418,#1423,#146,.T.);
#1744=EDGE_CURVE('',#1424,#1422,#1010,.T.);
#1745=EDGE_CURVE('',#1424,#1425,#1011,.T.);
#1746=EDGE_CURVE('',#1425,#1423,#1012,.T.);
#1747=EDGE_CURVE('',#1426,#1421,#1013,.T.);
#1748=EDGE_CURVE('',#1426,#1424,#1014,.T.);
#1749=EDGE_CURVE('',#1427,#1420,#1015,.T.);
#1750=EDGE_CURVE('',#1427,#1426,#1016,.T.);
#1751=EDGE_CURVE('',#1428,#1419,#1017,.T.);
#1752=EDGE_CURVE('',#1428,#1427,#1018,.T.);
#1753=EDGE_CURVE('',#1429,#1418,#1019,.T.);
#1754=EDGE_CURVE('',#1429,#1428,#1020,.T.);
#1755=EDGE_CURVE('',#1425,#1429,#1021,.T.);
#2282=ORIENTED_EDGE('',*,*,#1731,.F.);
#2283=ORIENTED_EDGE('',*,*,#1732,.T.);
#2284=ORIENTED_EDGE('',*,*,#1733,.F.);
#2285=ORIENTED_EDGE('',*,*,#1732,.F.);
#2286=ORIENTED_EDGE('',*,*,#1734,.F.);
#2287=ORIENTED_EDGE('',*,*,#1735,.T.);
#2288=ORIENTED_EDGE('',*,*,#1731,.T.);
#2289=ORIENTED_EDGE('',*,*,#1735,.F.);
#2290=ORIENTED_EDGE('',*,*,#1734,.T.);
#2291=ORIENTED_EDGE('',*,*,#1736,.F.);
#2292=ORIENTED_EDGE('',*,*,#1737,.T.);
#2293=ORIENTED_EDGE('',*,*,#1738,.F.);
#2294=ORIENTED_EDGE('',*,*,#1739,.F.);
#2295=ORIENTED_EDGE('',*,*,#1740,.F.);
#2296=ORIENTED_EDGE('',*,*,#1741,.F.);
#2297=ORIENTED_EDGE('',*,*,#1742,.F.);
#2298=ORIENTED_EDGE('',*,*,#1743,.F.);
#2299=ORIENTED_EDGE('',*,*,#1737,.F.);
#2300=ORIENTED_EDGE('',*,*,#1742,.T.);
#2301=ORIENTED_EDGE('',*,*,#1744,.F.);
#2302=ORIENTED_EDGE('',*,*,#1745,.T.);
#2303=ORIENTED_EDGE('',*,*,#1746,.T.);
#2304=ORIENTED_EDGE('',*,*,#1741,.T.);
#2305=ORIENTED_EDGE('',*,*,#1747,.F.);
#2306=ORIENTED_EDGE('',*,*,#1748,.T.);
#2307=ORIENTED_EDGE('',*,*,#1744,.T.);
#2308=ORIENTED_EDGE('',*,*,#1740,.T.);
#2309=ORIENTED_EDGE('',*,*,#1749,.F.);
#2310=ORIENTED_EDGE('',*,*,#1750,.T.);
#2311=ORIENTED_EDGE('',*,*,#1747,.T.);
#2312=ORIENTED_EDGE('',*,*,#1739,.T.);
#2313=ORIENTED_EDGE('',*,*,#1751,.F.);
#2314=ORIENTED_EDGE('',*,*,#1752,.T.);
#2315=ORIENTED_EDGE('',*,*,#1749,.T.);
#2316=ORIENTED_EDGE('',*,*,#1738,.T.);
#2317=ORIENTED_EDGE('',*,*,#1753,.F.);
#2318=ORIENTED_EDGE('',*,*,#1754,.T.);
#2319=ORIENTED_EDGE('',*,*,#1751,.T.);
#2320=ORIENTED_EDGE('',*,*,#1743,.T.);
#2321=ORIENTED_EDGE('',*,*,#1746,.F.);
#2322=ORIENTED_EDGE('',*,*,#1755,.T.);
#2323=ORIENTED_EDGE('',*,*,#1753,.T.);
#2324=ORIENTED_EDGE('',*,*,#1736,.T.);
#2325=ORIENTED_EDGE('',*,*,#1750,.F.);
#2326=ORIENTED_EDGE('',*,*,#1752,.F.);
#2327=ORIENTED_EDGE('',*,*,#1754,.F.);
#2328=ORIENTED_EDGE('',*,*,#1755,.F.);
#2329=ORIENTED_EDGE('',*,*,#1745,.F.);
#2330=ORIENTED_EDGE('',*,*,#1748,.F.);
#2331=ORIENTED_EDGE('',*,*,#1733,.T.);
#2755=PLANE('',#3332);
#2756=PLANE('',#3335);
#2757=PLANE('',#3336);
#2758=PLANE('',#3337);
#2759=PLANE('',#3338);
#2760=PLANE('',#3339);
#2761=PLANE('',#3340);
#2762=PLANE('',#3341);
#2763=PLANE('',#3342);
#2886=ADVANCED_FACE('',(#553),#272,.T.);
#2887=ADVANCED_FACE('',(#554),#162,.T.);
#2888=ADVANCED_FACE('',(#555),#2755,.T.);
#2889=ADVANCED_FACE('',(#556),#163,.T.);
#2890=ADVANCED_FACE('',(#557),#2756,.T.);
#2891=ADVANCED_FACE('',(#558),#2757,.T.);
#2892=ADVANCED_FACE('',(#559),#2758,.T.);
#2893=ADVANCED_FACE('',(#560),#2759,.T.);
#2894=ADVANCED_FACE('',(#561),#2760,.T.);
#2895=ADVANCED_FACE('',(#562),#2761,.T.);
#2896=ADVANCED_FACE('',(#563),#2762,.T.);
#2897=ADVANCED_FACE('',(#564,#320),#2763,.F.);
#2994=CLOSED_SHELL('',(#2886,#2887,#2888,#2889,#2890,#2891,#2892,#2893,
#2894,#2895,#2896,#2897));
#3326=AXIS2_PLACEMENT_3D('',#4864,#3943,#3944);
#3327=AXIS2_PLACEMENT_3D('',#4865,#3945,#3946);
#3328=AXIS2_PLACEMENT_3D('',#4867,#3947,#3948);
#3329=AXIS2_PLACEMENT_3D('',#4870,#3950,#3951);
#3330=AXIS2_PLACEMENT_3D('',#4871,#3952,#3953);
#3331=AXIS2_PLACEMENT_3D('',#4873,#3954,#3955);
#3332=AXIS2_PLACEMENT_3D('',#4875,#3957,#3958);
#3333=AXIS2_PLACEMENT_3D('',#4876,#3959,#3960);
#3334=AXIS2_PLACEMENT_3D('',#4878,#3961,#3962);
#3335=AXIS2_PLACEMENT_3D('',#4904,#3964,#3965);
#3336=AXIS2_PLACEMENT_3D('',#4910,#3969,#3970);
#3337=AXIS2_PLACEMENT_3D('',#4914,#3973,#3974);
#3338=AXIS2_PLACEMENT_3D('',#4918,#3977,#3978);
#3339=AXIS2_PLACEMENT_3D('',#4922,#3981,#3982);
#3340=AXIS2_PLACEMENT_3D('',#4926,#3985,#3986);
#3341=AXIS2_PLACEMENT_3D('',#4928,#3988,#3989);
#3342=AXIS2_PLACEMENT_3D('',#4929,#3990,#3991);
#3943=DIRECTION('axis',(0.,0.,1.));
#3944=DIRECTION('refdir',(1.,0.,0.));
#3945=DIRECTION('center_axis',(0.,-1.,0.));
#3946=DIRECTION('ref_axis',(1.,0.,0.));
#3947=DIRECTION('center_axis',(0.,1.,0.));
#3948=DIRECTION('ref_axis',(1.,0.,0.));
#3949=DIRECTION('',(0.,1.,0.));
#3950=DIRECTION('center_axis',(0.,-1.,0.));
#3951=DIRECTION('ref_axis',(1.,0.,0.));
#3952=DIRECTION('center_axis',(0.,1.,0.));
#3953=DIRECTION('ref_axis',(1.,0.,0.));
#3954=DIRECTION('center_axis',(0.,-1.,0.));
#3955=DIRECTION('ref_axis',(1.,0.,0.));
#3956=DIRECTION('',(-0.707106781186547,0.707106781186548,-8.65956056235493E-17));
#3957=DIRECTION('center_axis',(0.,-1.,0.));
#3958=DIRECTION('ref_axis',(0.,0.,-1.));
#3959=DIRECTION('center_axis',(0.,-1.,0.));
#3960=DIRECTION('ref_axis',(1.,0.,0.));
#3961=DIRECTION('center_axis',(0.,1.,0.));
#3962=DIRECTION('ref_axis',(1.,0.,0.));
#3963=DIRECTION('',(-0.866025403784439,-0.5,-1.06057523872491E-16));
#3964=DIRECTION('center_axis',(1.92296268638356E-16,0.,-1.));
#3965=DIRECTION('ref_axis',(-1.,0.,-1.92296268638356E-16));
#3966=DIRECTION('',(0.,1.,0.));
#3967=DIRECTION('',(-1.,0.,-1.92296268638356E-16));
#3968=DIRECTION('',(0.,1.,0.));
#3969=DIRECTION('center_axis',(0.866025403784439,0.,-0.5));
#3970=DIRECTION('ref_axis',(-0.5,0.,-0.866025403784439));
#3971=DIRECTION('',(0.,1.,0.));
#3972=DIRECTION('',(-0.5,0.,-0.866025403784439));
#3973=DIRECTION('center_axis',(0.866025403784439,0.,0.5));
#3974=DIRECTION('ref_axis',(0.5,0.,-0.866025403784439));
#3975=DIRECTION('',(0.,1.,0.));
#3976=DIRECTION('',(0.5,0.,-0.866025403784439));
#3977=DIRECTION('center_axis',(-1.92296268638356E-16,0.,1.));
#3978=DIRECTION('ref_axis',(1.,0.,1.92296268638356E-16));
#3979=DIRECTION('',(0.,1.,0.));
#3980=DIRECTION('',(1.,0.,1.92296268638356E-16));
#3981=DIRECTION('center_axis',(-0.866025403784439,0.,0.5));
#3982=DIRECTION('ref_axis',(0.5,0.,0.866025403784439));
#3983=DIRECTION('',(0.,1.,0.));
#3984=DIRECTION('',(0.5,0.,0.866025403784439));
#3985=DIRECTION('center_axis',(-0.866025403784439,0.,-0.5));
#3986=DIRECTION('ref_axis',(-0.5,0.,0.866025403784439));
#3987=DIRECTION('',(-0.5,0.,0.866025403784438));
#3988=DIRECTION('center_axis',(0.,1.,0.));
#3989=DIRECTION('ref_axis',(0.,0.,1.));
#3990=DIRECTION('center_axis',(0.,1.,0.));
#3991=DIRECTION('ref_axis',(1.,0.,0.));
#4864=CARTESIAN_POINT('',(0.,0.,0.));
#4865=CARTESIAN_POINT('Origin',(0.,-1.445,0.));
#4866=CARTESIAN_POINT('',(-0.2942,-2.9458,3.60291088309151E-17));
#4867=CARTESIAN_POINT('Origin',(0.,-2.9458,0.));
#4868=CARTESIAN_POINT('',(-0.2942,0.,-3.60291088309151E-17));
#4869=CARTESIAN_POINT('',(-0.2942,-1.445,-3.60291088309151E-17));
#4870=CARTESIAN_POINT('Origin',(0.,0.,0.));
#4871=CARTESIAN_POINT('Origin',(0.,-2.97,0.));
#4872=CARTESIAN_POINT('',(-0.24,-3.,-2.93915231795365E-17));
#4873=CARTESIAN_POINT('Origin',(0.,-3.,0.));
#4874=CARTESIAN_POINT('',(-0.27,-2.97,-3.30654635769785E-17));
#4875=CARTESIAN_POINT('Origin',(0.,-3.,0.));
#4876=CARTESIAN_POINT('Origin',(0.,0.341586508806388,0.));
#4877=CARTESIAN_POINT('',(-0.475,0.4,-5.81707229594993E-17));
#4878=CARTESIAN_POINT('Origin',(0.,0.4,0.));
#4879=CARTESIAN_POINT('',(-0.577350269189626,0.340908044531739,-7.07050159149938E-17));
#4880=CARTESIAN_POINT('',(-0.576175134594813,0.341586508806388,-7.05611034329833E-17));
#4881=CARTESIAN_POINT('',(-0.288675134594813,0.340908044531739,0.5));
#4882=CARTESIAN_POINT('Ctrl Pts',(-0.288675134594813,0.340908044531739,
0.5));
#4883=CARTESIAN_POINT('Ctrl Pts',(-0.433012701893303,0.424241377863696,
0.249999999998124));
#4884=CARTESIAN_POINT('Ctrl Pts',(-0.577350269189626,0.340908044531739,
-7.07050159149938E-17));
#4885=CARTESIAN_POINT('',(0.288675134594813,0.340908044531739,0.5));
#4886=CARTESIAN_POINT('Ctrl Pts',(0.288675134594813,0.340908044531739,0.5));
#4887=CARTESIAN_POINT('Ctrl Pts',(-2.16648921025353E-12,0.424241377863696,
0.5));
#4888=CARTESIAN_POINT('Ctrl Pts',(-0.288675134594813,0.340908044531739,
0.5));
#4889=CARTESIAN_POINT('',(0.577350269189626,0.340908044531739,0.));
#4890=CARTESIAN_POINT('Ctrl Pts',(0.577350269189626,0.340908044531739,0.));
#4891=CARTESIAN_POINT('Ctrl Pts',(0.433012701891136,0.424241377863697,0.250000000001876));
#4892=CARTESIAN_POINT('Ctrl Pts',(0.288675134594813,0.340908044531739,0.5));
#4893=CARTESIAN_POINT('',(0.288675134594813,0.340908044531739,-0.5));
#4894=CARTESIAN_POINT('Ctrl Pts',(0.288675134594813,0.340908044531739,-0.5));
#4895=CARTESIAN_POINT('Ctrl Pts',(0.433012701893303,0.424241377863696,-0.249999999998124));
#4896=CARTESIAN_POINT('Ctrl Pts',(0.577350269189626,0.340908044531739,0.));
#4897=CARTESIAN_POINT('',(-0.288675134594813,0.340908044531739,-0.5));
#4898=CARTESIAN_POINT('Ctrl Pts',(-0.288675134594813,0.340908044531739,
-0.5));
#4899=CARTESIAN_POINT('Ctrl Pts',(2.16660023255599E-12,0.424241377863696,
-0.5));
#4900=CARTESIAN_POINT('Ctrl Pts',(0.288675134594813,0.340908044531739,-0.5));
#4901=CARTESIAN_POINT('Ctrl Pts',(-0.577350269189626,0.340908044531739,
-7.07050159149938E-17));
#4902=CARTESIAN_POINT('Ctrl Pts',(-0.433012701891136,0.424241377863697,
-0.250000000001876));
#4903=CARTESIAN_POINT('Ctrl Pts',(-0.288675134594813,0.340908044531739,
-0.5));
#4904=CARTESIAN_POINT('Origin',(0.288675134594813,0.,-0.5));
#4905=CARTESIAN_POINT('',(0.288675134594813,0.,-0.5));
#4906=CARTESIAN_POINT('',(0.288675134594813,0.,-0.5));
#4907=CARTESIAN_POINT('',(-0.288675134594813,0.,-0.5));
#4908=CARTESIAN_POINT('',(0.288675134594813,0.,-0.5));
#4909=CARTESIAN_POINT('',(-0.288675134594813,0.,-0.5));
#4910=CARTESIAN_POINT('Origin',(0.577350269189626,0.,0.));
#4911=CARTESIAN_POINT('',(0.577350269189626,0.,0.));
#4912=CARTESIAN_POINT('',(0.577350269189626,0.,0.));
#4913=CARTESIAN_POINT('',(0.577350269189626,0.,0.));
#4914=CARTESIAN_POINT('Origin',(0.288675134594813,0.,0.5));
#4915=CARTESIAN_POINT('',(0.288675134594813,0.,0.5));
#4916=CARTESIAN_POINT('',(0.288675134594813,0.,0.5));
#4917=CARTESIAN_POINT('',(0.288675134594813,0.,0.5));
#4918=CARTESIAN_POINT('Origin',(-0.288675134594813,0.,0.5));
#4919=CARTESIAN_POINT('',(-0.288675134594813,0.,0.5));
#4920=CARTESIAN_POINT('',(-0.288675134594813,0.,0.5));
#4921=CARTESIAN_POINT('',(-0.288675134594813,0.,0.5));
#4922=CARTESIAN_POINT('Origin',(-0.577350269189626,0.,-7.07050159149938E-17));
#4923=CARTESIAN_POINT('',(-0.577350269189626,0.,-7.07050159149938E-17));
#4924=CARTESIAN_POINT('',(-0.577350269189626,0.,-7.07050159149938E-17));
#4925=CARTESIAN_POINT('',(-0.577350269189626,0.,-7.07050159149938E-17));
#4926=CARTESIAN_POINT('Origin',(-0.288675134594813,0.,-0.5));
#4927=CARTESIAN_POINT('',(-0.288675134594813,0.,-0.5));
#4928=CARTESIAN_POINT('Origin',(0.,0.4,0.));
#4929=CARTESIAN_POINT('Origin',(0.,0.,0.));
#5697=UNCERTAINTY_MEASURE_WITH_UNIT(LENGTH_MEASURE(0.001),#5735,
'DISTANCE_ACCURACY_VALUE',
'Maximum model space distance between geometric entities at asserted c
onnectivities');
#5711=UNCERTAINTY_MEASURE_WITH_UNIT(LENGTH_MEASURE(0.001),#5735,
'DISTANCE_ACCURACY_VALUE',
'Maximum model space distance between geometric entities at asserted c
onnectivities');
#5720=(
GEOMETRIC_REPRESENTATION_CONTEXT(3)
GLOBAL_UNCERTAINTY_ASSIGNED_CONTEXT((#5697))
GLOBAL_UNIT_ASSIGNED_CONTEXT((#5735,#5737,#5738))
REPRESENTATION_CONTEXT('','3D')
);
#5734=(
GEOMETRIC_REPRESENTATION_CONTEXT(3)
GLOBAL_UNCERTAINTY_ASSIGNED_CONTEXT((#5711))
GLOBAL_UNIT_ASSIGNED_CONTEXT((#5735,#5737,#5738))
REPRESENTATION_CONTEXT('','3D')
);
#5735=(
LENGTH_UNIT()
NAMED_UNIT(*)
SI_UNIT(.CENTI.,.METRE.)
);
#5737=(
NAMED_UNIT(*)
PLANE_ANGLE_UNIT()
SI_UNIT($,.RADIAN.)
);
#5738=(
NAMED_UNIT(*)
SI_UNIT($,.STERADIAN.)
SOLID_ANGLE_UNIT()
);
#5747=SHAPE_DEFINITION_REPRESENTATION(#5769,#5816);
#5769=PRODUCT_DEFINITION_SHAPE('',$,#5839);
#5816=SHAPE_REPRESENTATION('',(#3326),#5720);
#5830=PRODUCT_DEFINITION_CONTEXT('part definition',#5898,'design');
#5839=PRODUCT_DEFINITION('Hex Bolt - M6 x 30 mm',
'Hex Bolt - M6 x 30 mm',#5861,#5830);
#5861=PRODUCT_DEFINITION_FORMATION('',$,#5908);
#5898=APPLICATION_CONTEXT(
'Core Data for Automotive Mechanical Design Process');
#5899=PRODUCT_CONTEXT('part definition',#5898,'mechanical');
#5908=PRODUCT('Hex Bolt - M6 x 30 mm','Hex Bolt - M6 x 30 mm',
'Hex Bolt - M6 x 30 mm',(#5899));
#5985=COLOUR_RGB('Black',0.12,0.14,0.17);
#5986=FILL_AREA_STYLE_COLOUR('',#5985);
#5987=FILL_AREA_STYLE('',(#5986));
#5988=SURFACE_STYLE_FILL_AREA(#5987);
#5989=SURFACE_SIDE_STYLE('',(#5988));
#5990=SURFACE_STYLE_USAGE(.BOTH.,#5989);
#5991=PRESENTATION_STYLE_ASSIGNMENT((#5990));
ENDSEC;
END-ISO-10303-21;
